ISO-10303-21;
HEADER;
/* Generated by software containing ST-Developer
 * from STEP Tools, Inc. (www.steptools.com) 
 */

FILE_DESCRIPTION(
/* description */ ('Shaft runout checking stand'),
/* implementation_level */ '2;1');

FILE_NAME(
/* name */ 'M6x18 mounting screw.step',
/* time_stamp */ '2026-11-02T21:12:33-08:00',
/* author */ (''),
/* organization */ (''),
/* preprocessor_version */ 'ST-DEVELOPER v20.2',
/* originating_system */ 'Autodesk Translation Framework v15.17.0.0',
/* authorisation */ '');

FILE_SCHEMA (('AUTOMOTIVE_DESIGN { 1 0 10303 214 3 1 1 }'));
ENDSEC;

DATA;
#10=MECHANICAL_DESIGN_GEOMETRIC_PRESENTATION_REPRESENTATION('',(#478),#11748);
#353=ORIENTED_CLOSED_SHELL('',*,#6221,.F.);
#356=BREP_WITH_VOIDS('Body1',#6222,(#353));
#360=CONICAL_SURFACE('',#7011,0.475,0.785398163397449);
#361=CONICAL_SURFACE('',#7015,0.485,0.785398163397448);
#362=CONICAL_SURFACE('',#7019,0.31,0.463647609000806);
#392=SHAPE_REPRESENTATION_RELATIONSHIP('SRR','None',#11941,#435);
#435=ADVANCED_BREP_SHAPE_REPRESENTATION('',(#356),#11717);
#478=STYLED_ITEM('',(#12172),#356);
#621=FACE_BOUND('',#1637,.T.);
#760=CIRCLE('',#7008,0.2942);
#761=CIRCLE('',#7010,0.45);
#762=CIRCLE('',#7012,0.5);
#763=CIRCLE('',#7014,0.5);
#764=CIRCLE('',#7016,0.47);
#765=CIRCLE('',#7018,0.32);
#766=CIRCLE('',#7020,0.2942);
#980=CYLINDRICAL_SURFACE('',#7013,0.5);
#981=CYLINDRICAL_SURFACE('',#7021,0.2942);
#1196=FACE_OUTER_BOUND('',#1623,.T.);
#1197=FACE_OUTER_BOUND('',#1624,.T.);
#1198=FACE_OUTER_BOUND('',#1625,.T.);
#1199=FACE_OUTER_BOUND('',#1626,.T.);
#1200=FACE_OUTER_BOUND('',#1627,.T.);
#1201=FACE_OUTER_BOUND('',#1628,.T.);
#1202=FACE_OUTER_BOUND('',#1629,.T.);
#1203=FACE_OUTER_BOUND('',#1630,.T.);
#1204=FACE_OUTER_BOUND('',#1631,.T.);
#1205=FACE_OUTER_BOUND('',#1632,.T.);
#1206=FACE_OUTER_BOUND('',#1633,.T.);
#1207=FACE_OUTER_BOUND('',#1634,.T.);
#1208=FACE_OUTER_BOUND('',#1635,.T.);
#1209=FACE_OUTER_BOUND('',#1636,.T.);
#1210=FACE_OUTER_BOUND('',#1638,.T.);
#1211=FACE_OUTER_BOUND('',#1639,.T.);
#1623=EDGE_LOOP('',(#4836,#4837,#4838,#4839));
#1624=EDGE_LOOP('',(#4840,#4841,#4842,#4843));
#1625=EDGE_LOOP('',(#4844,#4845,#4846,#4847));
#1626=EDGE_LOOP('',(#4848,#4849,#4850,#4851));
#1627=EDGE_LOOP('',(#4852,#4853,#4854,#4855));
#1628=EDGE_LOOP('',(#4856,#4857,#4858,#4859));
#1629=EDGE_LOOP('',(#4860,#4861,#4862,#4863,#4864,#4865));
#1630=EDGE_LOOP('',(#4866,#4867,#4868,#4869,#4870,#4871));
#1631=EDGE_LOOP('',(#4872));
#1632=EDGE_LOOP('',(#4873));
#1633=EDGE_LOOP('',(#4874,#4875,#4876,#4877));
#1634=EDGE_LOOP('',(#4878,#4879,#4880,#4881));
#1635=EDGE_LOOP('',(#4882,#4883,#4884,#4885));
#1636=EDGE_LOOP('',(#4886));
#1637=EDGE_LOOP('',(#4887));
#1638=EDGE_LOOP('',(#4888,#4889,#4890,#4891));
#1639=EDGE_LOOP('',(#4892,#4893,#4894,#4895));
#2170=LINE('',#10277,#2637);
#2171=LINE('',#10279,#2638);
#2172=LINE('',#10281,#2639);
#2173=LINE('',#10282,#2640);
#2174=LINE('',#10285,#2641);
#2175=LINE('',#10287,#2642);
#2176=LINE('',#10288,#2643);
#2177=LINE('',#10291,#2644);
#2178=LINE('',#10293,#2645);
#2179=LINE('',#10294,#2646);
#2180=LINE('',#10297,#2647);
#2181=LINE('',#10299,#2648);
#2182=LINE('',#10300,#2649);
#2183=LINE('',#10303,#2650);
#2184=LINE('',#10305,#2651);
#2185=LINE('',#10306,#2652);
#2186=LINE('',#10308,#2653);
#2187=LINE('',#10309,#2654);
#2188=LINE('',#10321,#2655);
#2189=LINE('',#10325,#2656);
#2190=LINE('',#10329,#2657);
#2191=LINE('',#10336,#2658);
#2192=LINE('',#10338,#2659);
#2637=VECTOR('',#8309,1.);
#2638=VECTOR('',#8310,1.);
#2639=VECTOR('',#8311,1.);
#2640=VECTOR('',#8312,1.);
#2641=VECTOR('',#8315,1.);
#2642=VECTOR('',#8316,1.);
#2643=VECTOR('',#8317,1.);
#2644=VECTOR('',#8320,1.);
#2645=VECTOR('',#8321,1.);
#2646=VECTOR('',#8322,1.);
#2647=VECTOR('',#8325,1.);
#2648=VECTOR('',#8326,1.);
#2649=VECTOR('',#8327,1.);
#2650=VECTOR('',#8330,1.);
#2651=VECTOR('',#8331,1.);
#2652=VECTOR('',#8332,1.);
#2653=VECTOR('',#8335,1.);
#2654=VECTOR('',#8336,1.);
#2655=VECTOR('',#8353,0.475);
#2656=VECTOR('',#8358,0.5);
#2657=VECTOR('',#8363,0.485);
#2658=VECTOR('',#8372,0.31);
#2659=VECTOR('',#8375,0.3);
#3068=VERTEX_POINT('',#10275);
#3069=VERTEX_POINT('',#10276);
#3070=VERTEX_POINT('',#10278);
#3071=VERTEX_POINT('',#10280);
#3072=VERTEX_POINT('',#10284);
#3073=VERTEX_POINT('',#10286);
#3074=VERTEX_POINT('',#10290);
#3075=VERTEX_POINT('',#10292);
#3076=VERTEX_POINT('',#10296);
#3077=VERTEX_POINT('',#10298);
#3078=VERTEX_POINT('',#10302);
#3079=VERTEX_POINT('',#10304);
#3080=VERTEX_POINT('',#10313);
#3081=VERTEX_POINT('',#10316);
#3082=VERTEX_POINT('',#10319);
#3083=VERTEX_POINT('',#10323);
#3084=VERTEX_POINT('',#10327);
#3085=VERTEX_POINT('',#10331);
#3086=VERTEX_POINT('',#10334);
#3704=EDGE_CURVE('',#3068,#3069,#2170,.T.);
#3705=EDGE_CURVE('',#3069,#3070,#2171,.T.);
#3706=EDGE_CURVE('',#3070,#3071,#2172,.T.);
#3707=EDGE_CURVE('',#3068,#3071,#2173,.T.);
#3708=EDGE_CURVE('',#3069,#3072,#2174,.T.);
#3709=EDGE_CURVE('',#3072,#3073,#2175,.T.);
#3710=EDGE_CURVE('',#3073,#3070,#2176,.T.);
#3711=EDGE_CURVE('',#3072,#3074,#2177,.T.);
#3712=EDGE_CURVE('',#3074,#3075,#2178,.T.);
#3713=EDGE_CURVE('',#3075,#3073,#2179,.T.);
#3714=EDGE_CURVE('',#3074,#3076,#2180,.T.);
#3715=EDGE_CURVE('',#3076,#3077,#2181,.T.);
#3716=EDGE_CURVE('',#3077,#3075,#2182,.T.);
#3717=EDGE_CURVE('',#3076,#3078,#2183,.T.);
#3718=EDGE_CURVE('',#3078,#3079,#2184,.T.);
#3719=EDGE_CURVE('',#3079,#3077,#2185,.T.);
#3720=EDGE_CURVE('',#3078,#3068,#2186,.T.);
#3721=EDGE_CURVE('',#3071,#3079,#2187,.T.);
#3722=EDGE_CURVE('',#3080,#3080,#760,.T.);
#3723=EDGE_CURVE('',#3081,#3081,#761,.T.);
#3724=EDGE_CURVE('',#3082,#3082,#762,.T.);
#3725=EDGE_CURVE('',#3082,#3081,#2188,.T.);
#3726=EDGE_CURVE('',#3083,#3083,#763,.T.);
#3727=EDGE_CURVE('',#3083,#3082,#2189,.T.);
#3728=EDGE_CURVE('',#3084,#3084,#764,.T.);
#3729=EDGE_CURVE('',#3084,#3083,#2190,.T.);
#3730=EDGE_CURVE('',#3085,#3085,#765,.T.);
#3731=EDGE_CURVE('',#3086,#3086,#766,.F.);
#3732=EDGE_CURVE('',#3086,#3085,#2191,.T.);
#3733=EDGE_CURVE('',#3080,#3086,#2192,.T.);
#4836=ORIENTED_EDGE('',*,*,#3704,.T.);
#4837=ORIENTED_EDGE('',*,*,#3705,.T.);
#4838=ORIENTED_EDGE('',*,*,#3706,.T.);
#4839=ORIENTED_EDGE('',*,*,#3707,.F.);
#4840=ORIENTED_EDGE('',*,*,#3708,.T.);
#4841=ORIENTED_EDGE('',*,*,#3709,.T.);
#4842=ORIENTED_EDGE('',*,*,#3710,.T.);
#4843=ORIENTED_EDGE('',*,*,#3705,.F.);
#4844=ORIENTED_EDGE('',*,*,#3711,.T.);
#4845=ORIENTED_EDGE('',*,*,#3712,.T.);
#4846=ORIENTED_EDGE('',*,*,#3713,.T.);
#4847=ORIENTED_EDGE('',*,*,#3709,.F.);
#4848=ORIENTED_EDGE('',*,*,#3714,.T.);
#4849=ORIENTED_EDGE('',*,*,#3715,.T.);
#4850=ORIENTED_EDGE('',*,*,#3716,.T.);
#4851=ORIENTED_EDGE('',*,*,#3712,.F.);
#4852=ORIENTED_EDGE('',*,*,#3717,.T.);
#4853=ORIENTED_EDGE('',*,*,#3718,.T.);
#4854=ORIENTED_EDGE('',*,*,#3719,.T.);
#4855=ORIENTED_EDGE('',*,*,#3715,.F.);
#4856=ORIENTED_EDGE('',*,*,#3720,.T.);
#4857=ORIENTED_EDGE('',*,*,#3707,.T.);
#4858=ORIENTED_EDGE('',*,*,#3721,.T.);
#4859=ORIENTED_EDGE('',*,*,#3718,.F.);
#4860=ORIENTED_EDGE('',*,*,#3720,.F.);
#4861=ORIENTED_EDGE('',*,*,#3717,.F.);
#4862=ORIENTED_EDGE('',*,*,#3714,.F.);
#4863=ORIENTED_EDGE('',*,*,#3711,.F.);
#4864=ORIENTED_EDGE('',*,*,#3708,.F.);
#4865=ORIENTED_EDGE('',*,*,#3704,.F.);
#4866=ORIENTED_EDGE('',*,*,#3721,.F.);
#4867=ORIENTED_EDGE('',*,*,#3706,.F.);
#4868=ORIENTED_EDGE('',*,*,#3710,.F.);
#4869=ORIENTED_EDGE('',*,*,#3713,.F.);
#4870=ORIENTED_EDGE('',*,*,#3716,.F.);
#4871=ORIENTED_EDGE('',*,*,#3719,.F.);
#4872=ORIENTED_EDGE('',*,*,#3722,.F.);
#4873=ORIENTED_EDGE('',*,*,#3723,.F.);
#4874=ORIENTED_EDGE('',*,*,#3724,.F.);
#4875=ORIENTED_EDGE('',*,*,#3725,.T.);
#4876=ORIENTED_EDGE('',*,*,#3723,.T.);
#4877=ORIENTED_EDGE('',*,*,#3725,.F.);
#4878=ORIENTED_EDGE('',*,*,#3726,.F.);
#4879=ORIENTED_EDGE('',*,*,#3727,.T.);
#4880=ORIENTED_EDGE('',*,*,#3724,.T.);
#4881=ORIENTED_EDGE('',*,*,#3727,.F.);
#4882=ORIENTED_EDGE('',*,*,#3728,.F.);
#4883=ORIENTED_EDGE('',*,*,#3729,.T.);
#4884=ORIENTED_EDGE('',*,*,#3726,.T.);
#4885=ORIENTED_EDGE('',*,*,#3729,.F.);
#4886=ORIENTED_EDGE('',*,*,#3728,.T.);
#4887=ORIENTED_EDGE('',*,*,#3730,.F.);
#4888=ORIENTED_EDGE('',*,*,#3731,.F.);
#4889=ORIENTED_EDGE('',*,*,#3732,.T.);
#4890=ORIENTED_EDGE('',*,*,#3730,.T.);
#4891=ORIENTED_EDGE('',*,*,#3732,.F.);
#4892=ORIENTED_EDGE('',*,*,#3722,.T.);
#4893=ORIENTED_EDGE('',*,*,#3733,.T.);
#4894=ORIENTED_EDGE('',*,*,#3731,.T.);
#4895=ORIENTED_EDGE('',*,*,#3733,.F.);
#5719=PLANE('',#6999);
#5720=PLANE('',#7000);
#5721=PLANE('',#7001);
#5722=PLANE('',#7002);
#5723=PLANE('',#7003);
#5724=PLANE('',#7004);
#5725=PLANE('',#7005);
#5726=PLANE('',#7006);
#5727=PLANE('',#7007);
#5728=PLANE('',#7009);
#5729=PLANE('',#7017);
#5996=ADVANCED_FACE('',(#1196),#5719,.F.);
#5997=ADVANCED_FACE('',(#1197),#5720,.F.);
#5998=ADVANCED_FACE('',(#1198),#5721,.F.);
#5999=ADVANCED_FACE('',(#1199),#5722,.F.);
#6000=ADVANCED_FACE('',(#1200),#5723,.F.);
#6001=ADVANCED_FACE('',(#1201),#5724,.F.);
#6002=ADVANCED_FACE('',(#1202),#5725,.F.);
#6003=ADVANCED_FACE('',(#1203),#5726,.F.);
#6004=ADVANCED_FACE('',(#1204),#5727,.F.);
#6005=ADVANCED_FACE('',(#1205),#5728,.T.);
#6006=ADVANCED_FACE('',(#1206),#360,.T.);
#6007=ADVANCED_FACE('',(#1207),#980,.T.);
#6008=ADVANCED_FACE('',(#1208),#361,.T.);
#6009=ADVANCED_FACE('',(#1209,#621),#5729,.T.);
#6010=ADVANCED_FACE('',(#1210),#362,.T.);
#6011=ADVANCED_FACE('',(#1211),#981,.T.);
#6221=CLOSED_SHELL('',(#5996,#5997,#5998,#5999,#6000,#6001,#6002,#6003));
#6222=CLOSED_SHELL('',(#6004,#6005,#6006,#6007,#6008,#6009,#6010,#6011));
#6998=AXIS2_PLACEMENT_3D('',#10273,#8305,#8306);
#6999=AXIS2_PLACEMENT_3D('',#10274,#8307,#8308);
#7000=AXIS2_PLACEMENT_3D('',#10283,#8313,#8314);
#7001=AXIS2_PLACEMENT_3D('',#10289,#8318,#8319);
#7002=AXIS2_PLACEMENT_3D('',#10295,#8323,#8324);
#7003=AXIS2_PLACEMENT_3D('',#10301,#8328,#8329);
#7004=AXIS2_PLACEMENT_3D('',#10307,#8333,#8334);
#7005=AXIS2_PLACEMENT_3D('',#10310,#8337,#8338);
#7006=AXIS2_PLACEMENT_3D('',#10311,#8339,#8340);
#7007=AXIS2_PLACEMENT_3D('',#10312,#8341,#8342);
#7008=AXIS2_PLACEMENT_3D('',#10314,#8343,#8344);
#7009=AXIS2_PLACEMENT_3D('',#10315,#8345,#8346);
#7010=AXIS2_PLACEMENT_3D('',#10317,#8347,#8348);
#7011=AXIS2_PLACEMENT_3D('',#10318,#8349,#8350);
#7012=AXIS2_PLACEMENT_3D('',#10320,#8351,#8352);
#7013=AXIS2_PLACEMENT_3D('',#10322,#8354,#8355);
#7014=AXIS2_PLACEMENT_3D('',#10324,#8356,#8357);
#7015=AXIS2_PLACEMENT_3D('',#10326,#8359,#8360);
#7016=AXIS2_PLACEMENT_3D('',#10328,#8361,#8362);
#7017=AXIS2_PLACEMENT_3D('',#10330,#8364,#8365);
#7018=AXIS2_PLACEMENT_3D('',#10332,#8366,#8367);
#7019=AXIS2_PLACEMENT_3D('',#10333,#8368,#8369);
#7020=AXIS2_PLACEMENT_3D('',#10335,#8370,#8371);
#7021=AXIS2_PLACEMENT_3D('',#10337,#8373,#8374);
#8305=DIRECTION('axis',(0.,0.,1.));
#8306=DIRECTION('refdir',(1.,0.,0.));
#8307=DIRECTION('center_axis',(0.866025403784439,0.,-0.5));
#8308=DIRECTION('ref_axis',(0.5,0.,0.866025403784439));
#8309=DIRECTION('',(-0.5,0.,-0.866025403784439));
#8310=DIRECTION('',(0.,-1.,0.));
#8311=DIRECTION('',(0.5,0.,0.866025403784439));
#8312=DIRECTION('',(0.,-1.,0.));
#8313=DIRECTION('center_axis',(1.92296268638356E-16,0.,-1.));
#8314=DIRECTION('ref_axis',(1.,0.,1.92296268638356E-16));
#8315=DIRECTION('',(-1.,0.,-1.92296268638356E-16));
#8316=DIRECTION('',(0.,-1.,0.));
#8317=DIRECTION('',(1.,0.,1.92296268638356E-16));
#8318=DIRECTION('center_axis',(-0.866025403784439,0.,-0.5));
#8319=DIRECTION('ref_axis',(0.5,0.,-0.866025403784439));
#8320=DIRECTION('',(-0.5,0.,0.866025403784438));
#8321=DIRECTION('',(0.,-1.,0.));
#8322=DIRECTION('',(0.5,0.,-0.866025403784438));
#8323=DIRECTION('center_axis',(-0.866025403784439,0.,0.5));
#8324=DIRECTION('ref_axis',(-0.5,0.,-0.866025403784439));
#8325=DIRECTION('',(0.5,0.,0.866025403784439));
#8326=DIRECTION('',(0.,-1.,0.));
#8327=DIRECTION('',(-0.5,0.,-0.866025403784439));
#8328=DIRECTION('center_axis',(-1.92296268638356E-16,0.,1.));
#8329=DIRECTION('ref_axis',(-1.,0.,-1.92296268638356E-16));
#8330=DIRECTION('',(1.,0.,1.92296268638356E-16));
#8331=DIRECTION('',(0.,-1.,0.));
#8332=DIRECTION('',(-1.,0.,-1.92296268638356E-16));
#8333=DIRECTION('center_axis',(0.866025403784439,0.,0.5));
#8334=DIRECTION('ref_axis',(-0.5,0.,0.866025403784439));
#8335=DIRECTION('',(0.5,0.,-0.866025403784439));
#8336=DIRECTION('',(-0.5,0.,0.866025403784439));
#8337=DIRECTION('center_axis',(0.,1.,0.));
#8338=DIRECTION('ref_axis',(1.,0.,0.));
#8339=DIRECTION('center_axis',(0.,-1.,0.));
#8340=DIRECTION('ref_axis',(0.,0.,-1.));
#8341=DIRECTION('center_axis',(0.,1.,0.));
#8342=DIRECTION('ref_axis',(1.,0.,0.));
#8343=DIRECTION('center_axis',(0.,1.,0.));
#8344=DIRECTION('ref_axis',(1.,0.,0.));
#8345=DIRECTION('center_axis',(0.,1.,0.));
#8346=DIRECTION('ref_axis',(0.,0.,1.));
#8347=DIRECTION('center_axis',(0.,-1.,0.));
#8348=DIRECTION('ref_axis',(1.,0.,0.));
#8349=DIRECTION('center_axis',(0.,-1.,0.));
#8350=DIRECTION('ref_axis',(1.,0.,0.));
#8351=DIRECTION('center_axis',(0.,-1.,0.));
#8352=DIRECTION('ref_axis',(1.,0.,0.));
#8353=DIRECTION('',(0.707106781186548,0.707106781186547,8.65956056235494E-17));
#8354=DIRECTION('center_axis',(0.,-1.,0.));
#8355=DIRECTION('ref_axis',(1.,0.,0.));
#8356=DIRECTION('center_axis',(0.,-1.,0.));
#8357=DIRECTION('ref_axis',(1.,0.,0.));
#8358=DIRECTION('',(0.,1.,0.));
#8359=DIRECTION('center_axis',(0.,1.,0.));
#8360=DIRECTION('ref_axis',(1.,0.,0.));
#8361=DIRECTION('center_axis',(0.,-1.,0.));
#8362=DIRECTION('ref_axis',(1.,0.,0.));
#8363=DIRECTION('',(-0.707106781186547,0.707106781186548,-8.65956056235493E-17));
#8364=DIRECTION('center_axis',(0.,-1.,0.));
#8365=DIRECTION('ref_axis',(0.,0.,-1.));
#8366=DIRECTION('center_axis',(0.,-1.,0.));
#8367=DIRECTION('ref_axis',(1.,0.,0.));
#8368=DIRECTION('center_axis',(0.,1.,0.));
#8369=DIRECTION('ref_axis',(1.,0.,0.));
#8370=DIRECTION('center_axis',(0.,1.,0.));
#8371=DIRECTION('ref_axis',(1.,0.,0.));
#8372=DIRECTION('',(-0.447213595499958,0.894427190999916,-5.47678698264203E-17));
#8373=DIRECTION('center_axis',(0.,-1.,0.));
#8374=DIRECTION('ref_axis',(1.,0.,0.));
#8375=DIRECTION('',(0.,1.,0.));
#10273=CARTESIAN_POINT('',(0.,0.,0.));
#10274=CARTESIAN_POINT('Origin',(0.144337567297406,-0.6,-0.25));
#10275=CARTESIAN_POINT('',(0.288675134594813,-0.6,0.));
#10276=CARTESIAN_POINT('',(0.144337567297406,-0.6,-0.25));
#10277=CARTESIAN_POINT('',(0.288675134594813,-0.6,0.));
#10278=CARTESIAN_POINT('',(0.144337567297406,-0.96,-0.25));
#10279=CARTESIAN_POINT('',(0.144337567297406,-0.6,-0.25));
#10280=CARTESIAN_POINT('',(0.288675134594813,-0.96,0.));
#10281=CARTESIAN_POINT('',(0.288675134594813,-0.96,0.));
#10282=CARTESIAN_POINT('',(0.288675134594813,-0.6,0.));
#10283=CARTESIAN_POINT('Origin',(-0.144337567297406,-0.6,-0.25));
#10284=CARTESIAN_POINT('',(-0.144337567297406,-0.6,-0.25));
#10285=CARTESIAN_POINT('',(0.144337567297406,-0.6,-0.25));
#10286=CARTESIAN_POINT('',(-0.144337567297406,-0.96,-0.25));
#10287=CARTESIAN_POINT('',(-0.144337567297406,-0.6,-0.25));
#10288=CARTESIAN_POINT('',(0.144337567297406,-0.96,-0.25));
#10289=CARTESIAN_POINT('Origin',(-0.288675134594813,-0.6,-8.32667268468867E-17));
#10290=CARTESIAN_POINT('',(-0.288675134594813,-0.6,-3.53525079574969E-17));
#10291=CARTESIAN_POINT('',(-0.144337567297406,-0.6,-0.25));
#10292=CARTESIAN_POINT('',(-0.288675134594813,-0.96,-5.55111512312578E-17));
#10293=CARTESIAN_POINT('',(-0.288675134594813,-0.6,-3.53525079574969E-17));
#10294=CARTESIAN_POINT('',(-0.144337567297406,-0.96,-0.25));
#10295=CARTESIAN_POINT('Origin',(-0.144337567297407,-0.6,0.25));
#10296=CARTESIAN_POINT('',(-0.144337567297407,-0.6,0.25));
#10297=CARTESIAN_POINT('',(-0.288675134594813,-0.6,-3.53525079574969E-17));
#10298=CARTESIAN_POINT('',(-0.144337567297407,-0.96,0.25));
#10299=CARTESIAN_POINT('',(-0.144337567297407,-0.6,0.25));
#10300=CARTESIAN_POINT('',(-0.288675134594813,-0.96,-3.53525079574969E-17));
#10301=CARTESIAN_POINT('Origin',(0.144337567297406,-0.6,0.25));
#10302=CARTESIAN_POINT('',(0.144337567297406,-0.6,0.25));
#10303=CARTESIAN_POINT('',(-0.144337567297407,-0.6,0.25));
#10304=CARTESIAN_POINT('',(0.144337567297406,-0.96,0.25));
#10305=CARTESIAN_POINT('',(0.144337567297406,-0.6,0.25));
#10306=CARTESIAN_POINT('',(-0.144337567297407,-0.96,0.25));
#10307=CARTESIAN_POINT('Origin',(0.288675134594813,-0.6,0.));
#10308=CARTESIAN_POINT('',(0.144337567297406,-0.6,0.25));
#10309=CARTESIAN_POINT('',(0.144337567297406,-0.96,0.25));
#10310=CARTESIAN_POINT('Origin',(0.,-0.6,0.));
#10311=CARTESIAN_POINT('Origin',(0.,-0.96,0.));
#10312=CARTESIAN_POINT('Origin',(0.,-1.8,0.));
#10313=CARTESIAN_POINT('',(-0.2942,-1.8,3.60291088309151E-17));
#10314=CARTESIAN_POINT('Origin',(0.,-1.8,0.));
#10315=CARTESIAN_POINT('Origin',(0.45,0.6,0.));
#10316=CARTESIAN_POINT('',(-0.45,0.6,-5.51091059616309E-17));
#10317=CARTESIAN_POINT('Origin',(0.,0.6,0.));
#10318=CARTESIAN_POINT('Origin',(0.,0.575,0.));
#10319=CARTESIAN_POINT('',(-0.5,0.55,-6.12323399573677E-17));
#10320=CARTESIAN_POINT('Origin',(0.,0.55,0.));
#10321=CARTESIAN_POINT('',(-0.475,0.575,-5.81707229594993E-17));
#10322=CARTESIAN_POINT('Origin',(0.,0.29,0.));
#10323=CARTESIAN_POINT('',(-0.5,0.0299999999999998,-6.12323399573677E-17));
#10324=CARTESIAN_POINT('Origin',(0.,0.0299999999999998,0.));
#10325=CARTESIAN_POINT('',(-0.5,0.29,-6.12323399573677E-17));
#10326=CARTESIAN_POINT('Origin',(0.,0.0150000000000001,0.));
#10327=CARTESIAN_POINT('',(-0.47,7.11236625150491E-17,-5.75583995599256E-17));
#10328=CARTESIAN_POINT('Origin',(0.,0.,0.));
#10329=CARTESIAN_POINT('',(-0.485,0.0150000000000001,-5.93953697586466E-17));
#10330=CARTESIAN_POINT('Origin',(0.32,0.,0.));
#10331=CARTESIAN_POINT('',(-0.32,-6.93889390390723E-18,-3.91886975727153E-17));
#10332=CARTESIAN_POINT('Origin',(0.,0.,0.));
#10333=CARTESIAN_POINT('Origin',(0.,-0.02,0.));
#10334=CARTESIAN_POINT('',(-0.2942,-0.0515999999999999,3.60291088309151E-17));
#10335=CARTESIAN_POINT('Origin',(0.,-0.0515999999999999,0.));
#10336=CARTESIAN_POINT('',(-0.31,-0.02,-3.7964050773568E-17));
#10337=CARTESIAN_POINT('Origin',(0.,-1.24,0.));
#10338=CARTESIAN_POINT('',(-0.2942,-1.24,-3.60291088309151E-17));
#11668=UNCERTAINTY_MEASURE_WITH_UNIT(LENGTH_MEASURE(0.001),#11749,
'DISTANCE_ACCURACY_VALUE',
'Maximum model space distance between geometric entities at asserted c
onnectivities');
#11699=UNCERTAINTY_MEASURE_WITH_UNIT(LENGTH_MEASURE(0.001),#11749,
'DISTANCE_ACCURACY_VALUE',
'Maximum model space distance between geometric entities at asserted c
onnectivities');
#11717=(
GEOMETRIC_REPRESENTATION_CONTEXT(3)
GLOBAL_UNCERTAINTY_ASSIGNED_CONTEXT((#11668))
GLOBAL_UNIT_ASSIGNED_CONTEXT((#11749,#11751,#11752))
REPRESENTATION_CONTEXT('','3D')
);
#11748=(
GEOMETRIC_REPRESENTATION_CONTEXT(3)
GLOBAL_UNCERTAINTY_ASSIGNED_CONTEXT((#11699))
GLOBAL_UNIT_ASSIGNED_CONTEXT((#11749,#11751,#11752))
REPRESENTATION_CONTEXT('','3D')
);
#11749=(
LENGTH_UNIT()
NAMED_UNIT(*)
SI_UNIT(.CENTI.,.METRE.)
);
#11751=(
NAMED_UNIT(*)
PLANE_ANGLE_UNIT()
SI_UNIT($,.RADIAN.)
);
#11752=(
NAMED_UNIT(*)
SI_UNIT($,.STERADIAN.)
SOLID_ANGLE_UNIT()
);
#11770=SHAPE_DEFINITION_REPRESENTATION(#11818,#11941);
#11818=PRODUCT_DEFINITION_SHAPE('',$,#11990);
#11941=SHAPE_REPRESENTATION('',(#6998),#11717);
#11972=PRODUCT_DEFINITION_CONTEXT('part definition',#12118,'design');
#11990=PRODUCT_DEFINITION('M6x18 mounting screw','M6x18 mounting screw',
#12038,#11972);
#12038=PRODUCT_DEFINITION_FORMATION('',$,#12137);
#12118=APPLICATION_CONTEXT(
'Core Data for Automotive Mechanical Design Process');
#12119=PRODUCT_CONTEXT('part definition',#12118,'mechanical');
#12137=PRODUCT('M6x18 mounting screw','M6x18 mounting screw',
'M6x18 mounting screw',(#12119));
#12172=PRESENTATION_STYLE_ASSIGNMENT((#12177));
#12177=SURFACE_STYLE_USAGE(.BOTH.,#12182);
#12182=SURFACE_SIDE_STYLE('',(#12187));
#12187=SURFACE_STYLE_FILL_AREA(#12192);
#12192=FILL_AREA_STYLE('CAD Library Painted - Graphite',(#12197));
#12197=FILL_AREA_STYLE_COLOUR('CAD Library Painted - Graphite',#12202);
#12202=COLOUR_RGB('CAD Library Painted - Graphite',0.168627450980392,0.192156862745098,
0.231372549019608);
ENDSEC;
END-ISO-10303-21;
